ISO-10303-21;
HEADER;
FILE_DESCRIPTION (('STEP AP214'),
    '1' );
FILE_NAME ('16. Toe.step',
    '2026-10-09T14:04:53',
    ( '' ),
    ( '' ),
    'SwSTEP 2.0',
    'SolidWorks 2021',
    '' );
FILE_SCHEMA (( 'AUTOMOTIVE_DESIGN' ));
ENDSEC;

DATA;
#763=STYLED_ITEM ( 'NONE', ( #7839 ), #82029 ) ;
#1039=CARTESIAN_POINT ( 'NONE',  ( 0.000000000000000000, 3.500000000000000000, -4.000000000000000000 ) ) ;
#1437=CYLINDRICAL_SURFACE ( 'NONE', #33669, 2.000000000000000444 ) ;
#2912=STYLED_ITEM ( 'NONE', ( #8871 ), #23880 ) ;
#3018=UNCERTAINTY_MEASURE_WITH_UNIT (LENGTH_MEASURE( 1.000000000000000082E-05 ), #42303, 'distance_accuracy_value', 'NONE');
#3575=ADVANCED_FACE ( 'NONE', ( #74722 ), #45966, .T. ) ;
#3718=ORIENTED_EDGE ( 'NONE', *, *, #26732, .F. ) ;
#4386=COLOUR_RGB ( '', 0.08235294, 0.09019608, 0.10196078) ;
#4405=PRODUCT_CONTEXT ( 'NONE', #102408, 'mechanical' ) ;
#4846=FILL_AREA_STYLE ('',( #79254 ) ) ;
#4936=LINE ( 'NONE', #94490, #20461 ) ;
#5480=AXIS2_PLACEMENT_3D ( 'NONE', #15270, #72443, #23389 ) ;
#5565=DIRECTION ( 'NONE',  ( 0.000000000000000000, 0.000000000000000000, -1.000000000000000000 ) ) ;
#5955=( GEOMETRIC_REPRESENTATION_CONTEXT ( 3 ) GLOBAL_UNCERTAINTY_ASSIGNED_CONTEXT ( ( #84472 ) ) GLOBAL_UNIT_ASSIGNED_CONTEXT ( ( #56380, #65560, #32693 ) ) REPRESENTATION_CONTEXT ( 'NONE', 'WORKASPACE' ) );
#6049=DIRECTION ( 'NONE',  ( -1.000000000000000000, 0.000000000000000000, 0.000000000000000000 ) ) ;
#6294=CARTESIAN_POINT ( 'NONE',  ( 0.000000000000000000, 0.000000000000000000, 0.000000000000000000 ) ) ;
#6702=PRODUCT_DEFINITION ( 'UNKNOWN', '', #12803, #72647 ) ;
#6882=ORIENTED_EDGE ( 'NONE', *, *, #82406, .T. ) ;
#7082=CIRCLE ( 'NONE', #79385, 4.000000000000000000 ) ;
#7107=ORIENTED_EDGE ( 'NONE', *, *, #71450, .T. ) ;
#7304=SURFACE_SIDE_STYLE ('',( #29650 ) ) ;
#7360=DIRECTION ( 'NONE',  ( 0.000000000000000000, 0.000000000000000000, -1.000000000000000000 ) ) ;
#7475=FACE_OUTER_BOUND ( 'NONE', #80688, .T. ) ;
#7587=SURFACE_SIDE_STYLE ('',( #57203 ) ) ;
#7839=PRESENTATION_STYLE_ASSIGNMENT (( #15945 ) ) ;
#7969=LINE ( 'NONE', #10106, #95271 ) ;
#8068=MECHANICAL_DESIGN_GEOMETRIC_PRESENTATION_REPRESENTATION('',(#2912),#92454);
#8663=( LENGTH_UNIT ( ) NAMED_UNIT ( * ) SI_UNIT ( .MILLI., .METRE. ) );
#8871=PRESENTATION_STYLE_ASSIGNMENT (( #82768 ) ) ;
#9326=MECHANICAL_DESIGN_GEOMETRIC_PRESENTATION_REPRESENTATION('',(#763),#5955);
#9673=AXIS2_PLACEMENT_3D ( 'NONE', #32115, #39678, #64997 ) ;
#9750=MECHANICAL_DESIGN_GEOMETRIC_PRESENTATION_REPRESENTATION('',(#102791),#99289);
#10081=DIRECTION ( 'NONE',  ( 0.000000000000000000, 0.000000000000000000, -1.000000000000000000 ) ) ;
#10091=VERTEX_POINT ( 'NONE', #102810 ) ;
#10106=CARTESIAN_POINT ( 'NONE',  ( 0.000000000000000000, 0.000000000000000000, -4.000000000000000000 ) ) ;
#10370=ORIENTED_EDGE ( 'NONE', *, *, #39415, .F. ) ;
#10728=AXIS2_PLACEMENT_3D ( 'NONE', #14983, #57033, #47878 ) ;
#12154=EDGE_CURVE ( 'NONE', #24916, #70311, #69077, .T. ) ;
#12216=DIRECTION ( 'NONE',  ( 0.000000000000000000, 0.000000000000000000, -1.000000000000000000 ) ) ;
#12612=STYLED_ITEM ( 'NONE', ( #20543 ), #54542 ) ;
#12803=PRODUCT_DEFINITION_FORMATION_WITH_SPECIFIED_SOURCE ( 'ANY', '', #43795, .NOT_KNOWN. ) ;
#12915=( LENGTH_UNIT ( ) NAMED_UNIT ( * ) SI_UNIT ( .MILLI., .METRE. ) );
#13453=CARTESIAN_POINT ( 'NONE',  ( 0.000000000000000000, 0.000000000000000000, 0.000000000000000000 ) ) ;
#13648=DIRECTION ( 'NONE',  ( -0.000000000000000000, -1.000000000000000000, -0.000000000000000000 ) ) ;
#13711=CIRCLE ( 'NONE', #74931, 2.000000000000000888 ) ;
#13838=CARTESIAN_POINT ( 'NONE',  ( 0.000000000000000000, 0.000000000000000000, -3.500000000000000000 ) ) ;
#14338=FACE_OUTER_BOUND ( 'NONE', #62072, .T. ) ;
#14974=AXIS2_PLACEMENT_3D ( 'NONE', #73477, #90213, #23381 ) ;
#14983=CARTESIAN_POINT ( 'NONE',  ( 0.000000000000000000, 0.000000000000000000, 0.000000000000000000 ) ) ;
#15270=CARTESIAN_POINT ( 'NONE',  ( 0.000000000000000000, 4.000000000000000000, 0.000000000000000000 ) ) ;
#15679=EDGE_LOOP ( 'NONE', ( #28655, #95189, #103443, #49460 ) ) ;
#15695=UNCERTAINTY_MEASURE_WITH_UNIT (LENGTH_MEASURE( 1.000000000000000082E-05 ), #8663, 'distance_accuracy_value', 'NONE');
#15709=EDGE_LOOP ( 'NONE', ( #64348, #35106 ) ) ;
#15945=SURFACE_STYLE_USAGE ( .BOTH. , #7304 ) ;
#17440=( LENGTH_UNIT ( ) NAMED_UNIT ( * ) SI_UNIT ( .MILLI., .METRE. ) );
#17797=DIRECTION ( 'NONE',  ( -0.000000000000000000, -1.000000000000000000, -0.000000000000000000 ) ) ;
#18552=EDGE_LOOP ( 'NONE', ( #31046, #59584 ) ) ;
#19609=MECHANICAL_DESIGN_GEOMETRIC_PRESENTATION_REPRESENTATION('',(#12612),#83222);
#19727=DIRECTION ( 'NONE',  ( 0.000000000000000000, 0.000000000000000000, 1.000000000000000000 ) ) ;
#19743=PRESENTATION_STYLE_ASSIGNMENT (( #25710 ) ) ;
#19842=AXIS2_PLACEMENT_3D ( 'NONE', #50981, #59641, #36982 ) ;
#19997=DIRECTION ( 'NONE',  ( 0.000000000000000000, 1.000000000000000000, 0.000000000000000000 ) ) ;
#20461=VECTOR ( 'NONE', #78280, 1000.000000000000000 ) ;
#20543=PRESENTATION_STYLE_ASSIGNMENT (( #29153 ) ) ;
#21788=( NAMED_UNIT ( * ) SI_UNIT ( $, .STERADIAN. ) SOLID_ANGLE_UNIT ( ) );
#22031=SHAPE_REPRESENTATION ( '16. Toe', ( #10728 ), #26637 ) ;
#22099=ORIENTED_EDGE ( 'NONE', *, *, #88968, .T. ) ;
#22109=SURFACE_STYLE_FILL_AREA ( #4846 ) ;
#22708=CARTESIAN_POINT ( 'NONE',  ( 4.898587196589412829E-16, 0.5000000000000000000, 4.000000000000000000 ) ) ;
#22914=CARTESIAN_POINT ( 'NONE',  ( 4.592425496802573972E-16, 4.000000000000000000, -3.500000000000000000 ) ) ;
#23044=DIRECTION ( 'NONE',  ( 0.000000000000000000, 0.000000000000000000, -1.000000000000000000 ) ) ;
#23381=DIRECTION ( 'NONE',  ( 0.000000000000000000, -0.000000000000000000, 1.000000000000000000 ) ) ;
#23389=DIRECTION ( 'NONE',  ( 0.000000000000000000, 0.000000000000000000, -1.000000000000000000 ) ) ;
#23804=SHAPE_DEFINITION_REPRESENTATION ( #77403, #22031 ) ;
#23832=FILL_AREA_STYLE_COLOUR ( '', #76442 ) ;
#23880=ADVANCED_FACE ( 'NONE', ( #74658 ), #85627, .T. ) ;
#23987=CARTESIAN_POINT ( 'NONE',  ( 0.000000000000000000, 12.00000000000000000, -2.000000000000000000 ) ) ;
#24141=UNCERTAINTY_MEASURE_WITH_UNIT (LENGTH_MEASURE( 1.000000000000000082E-05 ), #56916, 'distance_accuracy_value', 'NONE');
#24217=DIRECTION ( 'NONE',  ( -0.000000000000000000, -1.000000000000000000, -0.000000000000000000 ) ) ;
#24242=AXIS2_PLACEMENT_3D ( 'NONE', #13453, #89489, #47937 ) ;
#24600=DIRECTION ( 'NONE',  ( 0.000000000000000000, 1.000000000000000000, 0.000000000000000000 ) ) ;
#24820=MECHANICAL_DESIGN_GEOMETRIC_PRESENTATION_REPRESENTATION('',(#90237),#59303);
#24916=VERTEX_POINT ( 'NONE', #1039 ) ;
#25254=APPLICATION_CONTEXT ( 'automotive_design' ) ;
#25710=SURFACE_STYLE_USAGE ( .BOTH. , #33775 ) ;
#25812=CIRCLE ( 'NONE', #53325, 0.5000000000000000000 ) ;
#26344=VERTEX_POINT ( 'NONE', #34861 ) ;
#26454=AXIS2_PLACEMENT_3D ( 'NONE', #61489, #19997, #85765 ) ;
#26637=( GEOMETRIC_REPRESENTATION_CONTEXT ( 3 ) GLOBAL_UNCERTAINTY_ASSIGNED_CONTEXT ( ( #24141 ) ) GLOBAL_UNIT_ASSIGNED_CONTEXT ( ( #56916, #49358, #106538 ) ) REPRESENTATION_CONTEXT ( 'NONE', 'WORKASPACE' ) );
#26732=EDGE_CURVE ( 'NONE', #70311, #80736, #85773, .T. ) ;
#26979=CIRCLE ( 'NONE', #9673, 2.000000000000000000 ) ;
#27236=FILL_AREA_STYLE ('',( #42841 ) ) ;
#28300=DIRECTION ( 'NONE',  ( 1.000000000000000000, 0.000000000000000000, -1.224646799147353207E-16 ) ) ;
#28607=SURFACE_SIDE_STYLE ('',( #69044 ) ) ;
#28626=SURFACE_STYLE_USAGE ( .BOTH. , #94937 ) ;
#28655=ORIENTED_EDGE ( 'NONE', *, *, #56417, .T. ) ;
#29153=SURFACE_STYLE_USAGE ( .BOTH. , #28607 ) ;
#29650=SURFACE_STYLE_FILL_AREA ( #98965 ) ;
#29777=ORIENTED_EDGE ( 'NONE', *, *, #83427, .T. ) ;
#30410=FACE_BOUND ( 'NONE', #80610, .T. ) ;
#30730=AXIS2_PLACEMENT_3D ( 'NONE', #37792, #56026, #87379 ) ;
#31046=ORIENTED_EDGE ( 'NONE', *, *, #57990, .T. ) ;
#31712=EDGE_LOOP ( 'NONE', ( #106688, #38738, #7107, #3718 ) ) ;
#31765=CARTESIAN_POINT ( 'NONE',  ( 0.000000000000000000, 0.000000000000000000, 0.000000000000000000 ) ) ;
#31941=ORIENTED_EDGE ( 'NONE', *, *, #88968, .F. ) ;
#32115=CARTESIAN_POINT ( 'NONE',  ( 0.000000000000000000, 12.00000000000000000, 0.000000000000000000 ) ) ;
#32693=( NAMED_UNIT ( * ) SI_UNIT ( $, .STERADIAN. ) SOLID_ANGLE_UNIT ( ) );
#33346=DIRECTION ( 'NONE',  ( -0.000000000000000000, -1.000000000000000000, -0.000000000000000000 ) ) ;
#33362=TOROIDAL_SURFACE ( 'NONE', #26454, 3.500000000000000000, 0.5000000000000000000 ) ;
#33669=AXIS2_PLACEMENT_3D ( 'NONE', #51053, #83970, #10081 ) ;
#33775=SURFACE_SIDE_STYLE ('',( #83357 ) ) ;
#34096=CIRCLE ( 'NONE', #63338, 0.5000000000000000000 ) ;
#34861=CARTESIAN_POINT ( 'NONE',  ( 4.898587196589412829E-16, 3.500000000000000000, 4.000000000000000000 ) ) ;
#34895=ORIENTED_EDGE ( 'NONE', *, *, #84976, .F. ) ;
#34943=FACE_OUTER_BOUND ( 'NONE', #94842, .T. ) ;
#35053=VERTEX_POINT ( 'NONE', #13838 ) ;
#35106=ORIENTED_EDGE ( 'NONE', *, *, #26732, .T. ) ;
#35216=AXIS2_PLACEMENT_3D ( 'NONE', #41568, #97142, #72346 ) ;
#35858=SURFACE_STYLE_FILL_AREA ( #27236 ) ;
#35884=AXIS2_PLACEMENT_3D ( 'NONE', #86035, #60690, #19727 ) ;
#36120=ORIENTED_EDGE ( 'NONE', *, *, #100801, .F. ) ;
#36177=AXIS2_PLACEMENT_3D ( 'NONE', #44692, #93761, #60872 ) ;
#36926=VECTOR ( 'NONE', #88539, 1000.000000000000000 ) ;
#36982=DIRECTION ( 'NONE',  ( 0.000000000000000000, 0.000000000000000000, 1.000000000000000000 ) ) ;
#37414=CARTESIAN_POINT ( 'NONE',  ( 0.000000000000000000, 3.500000000000000000, 3.500000000000000000 ) ) ;
#37516=( NAMED_UNIT ( * ) PLANE_ANGLE_UNIT ( ) SI_UNIT ( $, .RADIAN. ) );
#37564=DIRECTION ( 'NONE',  ( 0.000000000000000000, 0.000000000000000000, -1.000000000000000000 ) ) ;
#37780=( NAMED_UNIT ( * ) SI_UNIT ( $, .STERADIAN. ) SOLID_ANGLE_UNIT ( ) );
#37792=CARTESIAN_POINT ( 'NONE',  ( 0.000000000000000000, 4.000000000000000000, 0.000000000000000000 ) ) ;
#38309=CYLINDRICAL_SURFACE ( 'NONE', #24242, 4.000000000000000000 ) ;
#38501=FACE_OUTER_BOUND ( 'NONE', #15709, .T. ) ;
#38656=DIRECTION ( 'NONE',  ( 0.000000000000000000, -0.000000000000000000, 1.000000000000000000 ) ) ;
#38701=DIRECTION ( 'NONE',  ( -0.000000000000000000, -1.000000000000000000, -0.000000000000000000 ) ) ;
#38738=ORIENTED_EDGE ( 'NONE', *, *, #81699, .F. ) ;
#39234=FACE_OUTER_BOUND ( 'NONE', #15679, .T. ) ;
#39415=EDGE_CURVE ( 'NONE', #26344, #49975, #4936, .T. ) ;
#39678=DIRECTION ( 'NONE',  ( -0.000000000000000000, -1.000000000000000000, -0.000000000000000000 ) ) ;
#39994=DIRECTION ( 'NONE',  ( -0.000000000000000000, -1.000000000000000000, -0.000000000000000000 ) ) ;
#40167=CARTESIAN_POINT ( 'NONE',  ( 4.286263797015736595E-16, 3.500000000000000000, -3.500000000000000000 ) ) ;
#41137=PLANE ( 'NONE',  #14974 ) ;
#41350=EDGE_LOOP ( 'NONE', ( #96137, #91918, #99906, #65183 ) ) ;
#41568=CARTESIAN_POINT ( 'NONE',  ( 0.000000000000000000, 3.500000000000000000, 0.000000000000000000 ) ) ;
#42254=CIRCLE ( 'NONE', #56009, 2.000000000000000000 ) ;
#42303=( LENGTH_UNIT ( ) NAMED_UNIT ( * ) SI_UNIT ( .MILLI., .METRE. ) );
#42369=FILL_AREA_STYLE ('',( #50445 ) ) ;
#42841=FILL_AREA_STYLE_COLOUR ( '', #76983 ) ;
#43192=AXIS2_PLACEMENT_3D ( 'NONE', #40167, #88204, #49302 ) ;
#43795=PRODUCT ( '16. Toe', '16. Toe', '', ( #4405 ) ) ;
#43861=ORIENTED_EDGE ( 'NONE', *, *, #57990, .F. ) ;
#44169=EDGE_LOOP ( 'NONE', ( #36120, #75096, #43861, #96894 ) ) ;
#44692=CARTESIAN_POINT ( 'NONE',  ( 0.000000000000000000, 0.5000000000000000000, 0.000000000000000000 ) ) ;
#44798=DIRECTION ( 'NONE',  ( -0.000000000000000000, -1.000000000000000000, -0.000000000000000000 ) ) ;
#45324=CARTESIAN_POINT ( 'NONE',  ( 0.000000000000000000, 12.00000000000000000, 0.000000000000000000 ) ) ;
#45966=TOROIDAL_SURFACE ( 'NONE', #51175, 3.500000000000000000, 0.5000000000000000000 ) ;
#46105=( NAMED_UNIT ( * ) SI_UNIT ( $, .STERADIAN. ) SOLID_ANGLE_UNIT ( ) );
#46398=CARTESIAN_POINT ( 'NONE',  ( 0.000000000000000000, 0.5000000000000000000, 0.000000000000000000 ) ) ;
#46911=DIRECTION ( 'NONE',  ( 0.000000000000000000, 1.000000000000000000, 0.000000000000000000 ) ) ;
#47528=CARTESIAN_POINT ( 'NONE',  ( 0.000000000000000000, 0.000000000000000000, -2.000000000000000444 ) ) ;
#47544=DIRECTION ( 'NONE',  ( 0.000000000000000000, -1.000000000000000000, -0.000000000000000000 ) ) ;
#47639=CARTESIAN_POINT ( 'NONE',  ( 2.449293598294706907E-16, 12.00000000000000000, 2.000000000000000000 ) ) ;
#47878=DIRECTION ( 'NONE',  ( 1.000000000000000000, 0.000000000000000000, 0.000000000000000000 ) ) ;
#47937=DIRECTION ( 'NONE',  ( 0.000000000000000000, 0.000000000000000000, -1.000000000000000000 ) ) ;
#48711=EDGE_CURVE ( 'NONE', #94714, #49975, #67170, .T. ) ;
#49126=EDGE_CURVE ( 'NONE', #91320, #58206, #13711, .T. ) ;
#49302=DIRECTION ( 'NONE',  ( 1.224646799147352468E-16, 0.000000000000000000, -1.000000000000000000 ) ) ;
#49358=( NAMED_UNIT ( * ) PLANE_ANGLE_UNIT ( ) SI_UNIT ( $, .RADIAN. ) );
#49460=ORIENTED_EDGE ( 'NONE', *, *, #55231, .F. ) ;
#49485=AXIS2_PLACEMENT_3D ( 'NONE', #88556, #47544, #64803 ) ;
#49975=VERTEX_POINT ( 'NONE', #22708 ) ;
#50308=( NAMED_UNIT ( * ) PLANE_ANGLE_UNIT ( ) SI_UNIT ( $, .RADIAN. ) );
#50445=FILL_AREA_STYLE_COLOUR ( '', #61456 ) ;
#50449=EDGE_CURVE ( 'NONE', #96436, #91320, #72033, .T. ) ;
#50821=CARTESIAN_POINT ( 'NONE',  ( 0.000000000000000000, 3.500000000000000000, 0.000000000000000000 ) ) ;
#50981=CARTESIAN_POINT ( 'NONE',  ( 0.000000000000000000, 0.5000000000000000000, -3.500000000000000000 ) ) ;
#51053=CARTESIAN_POINT ( 'NONE',  ( 0.000000000000000000, 0.000000000000000000, 0.000000000000000000 ) ) ;
#51175=AXIS2_PLACEMENT_3D ( 'NONE', #105776, #39994, #78988 ) ;
#51192=CARTESIAN_POINT ( 'NONE',  ( 0.000000000000000000, 3.500000000000000000, 0.000000000000000000 ) ) ;
#52840=FACE_OUTER_BOUND ( 'NONE', #31712, .T. ) ;
#53325=AXIS2_PLACEMENT_3D ( 'NONE', #37414, #6049, #54060 ) ;
#53401=( NAMED_UNIT ( * ) PLANE_ANGLE_UNIT ( ) SI_UNIT ( $, .RADIAN. ) );
#54060=DIRECTION ( 'NONE',  ( 0.000000000000000000, 0.000000000000000000, 1.000000000000000000 ) ) ;
#54516=AXIS2_PLACEMENT_3D ( 'NONE', #46398, #46911, #104621 ) ;
#54542=ADVANCED_FACE ( 'NONE', ( #52840 ), #33362, .T. ) ;
#54550=CIRCLE ( 'NONE', #83909, 3.500000000000000000 ) ;
#54622=( NAMED_UNIT ( * ) PLANE_ANGLE_UNIT ( ) SI_UNIT ( $, .RADIAN. ) );
#55172=ADVANCED_FACE ( 'NONE', ( #79372 ), #69616, .T. ) ;
#55231=EDGE_CURVE ( 'NONE', #70351, #58206, #64785, .T. ) ;
#55718=AXIS2_PLACEMENT_3D ( 'NONE', #63497, #87235, #23044 ) ;
#55803=EDGE_CURVE ( 'NONE', #94714, #35053, #85226, .T. ) ;
#55829=COLOUR_RGB ( '', 0.08235294, 0.09019608, 0.10196078) ;
#56009=AXIS2_PLACEMENT_3D ( 'NONE', #45324, #44798, #95993 ) ;
#56026=DIRECTION ( 'NONE',  ( 0.000000000000000000, 1.000000000000000000, 0.000000000000000000 ) ) ;
#56126=FILL_AREA_STYLE ('',( #23832 ) ) ;
#56380=( LENGTH_UNIT ( ) NAMED_UNIT ( * ) SI_UNIT ( .MILLI., .METRE. ) );
#56417=EDGE_CURVE ( 'NONE', #70351, #96436, #42254, .T. ) ;
#56916=( LENGTH_UNIT ( ) NAMED_UNIT ( * ) SI_UNIT ( .MILLI., .METRE. ) );
#56944=ADVANCED_FACE ( 'NONE', ( #39234 ), #83778, .T. ) ;
#57033=DIRECTION ( 'NONE',  ( 0.000000000000000000, 0.000000000000000000, 1.000000000000000000 ) ) ;
#57203=SURFACE_STYLE_FILL_AREA ( #56126 ) ;
#57475=ORIENTED_EDGE ( 'NONE', *, *, #81699, .T. ) ;
#57710=MECHANICAL_DESIGN_GEOMETRIC_PRESENTATION_REPRESENTATION('',(#104232),#92208);
#57990=EDGE_CURVE ( 'NONE', #35053, #10091, #54550, .T. ) ;
#58206=VERTEX_POINT ( 'NONE', #68375 ) ;
#58415=FILL_AREA_STYLE ('',( #102459 ) ) ;
#58777=VECTOR ( 'NONE', #104940, 1000.000000000000000 ) ;
#59149=COLOUR_RGB ( '', 0.09019608, 0.27058824, 0.51372549) ;
#59200=CYLINDRICAL_SURFACE ( 'NONE', #73631, 4.000000000000000000 ) ;
#59303=( GEOMETRIC_REPRESENTATION_CONTEXT ( 3 ) GLOBAL_UNCERTAINTY_ASSIGNED_CONTEXT ( ( #15695 ) ) GLOBAL_UNIT_ASSIGNED_CONTEXT ( ( #8663, #74453, #105248 ) ) REPRESENTATION_CONTEXT ( 'NONE', 'WORKASPACE' ) );
#59584=ORIENTED_EDGE ( 'NONE', *, *, #84976, .T. ) ;
#59641=DIRECTION ( 'NONE',  ( -1.000000000000000000, 0.000000000000000000, 0.000000000000000000 ) ) ;
#60242=ADVANCED_FACE ( 'NONE', ( #63228 ), #63758, .T. ) ;
#60690=DIRECTION ( 'NONE',  ( 0.000000000000000000, 1.000000000000000000, 0.000000000000000000 ) ) ;
#60872=DIRECTION ( 'NONE',  ( 0.000000000000000000, 0.000000000000000000, -1.000000000000000000 ) ) ;
#61175=DIRECTION ( 'NONE',  ( -1.224646799147353454E-16, 0.000000000000000000, -1.000000000000000000 ) ) ;
#61456=COLOUR_RGB ( '', 0.08235294, 0.09019608, 0.10196078) ;
#61489=CARTESIAN_POINT ( 'NONE',  ( 0.000000000000000000, 3.500000000000000000, 0.000000000000000000 ) ) ;
#61507=PRESENTATION_STYLE_ASSIGNMENT (( #28626 ) ) ;
#62024=( NAMED_UNIT ( * ) SI_UNIT ( $, .STERADIAN. ) SOLID_ANGLE_UNIT ( ) );
#62072=EDGE_LOOP ( 'NONE', ( #69396, #31941 ) ) ;
#63228=FACE_OUTER_BOUND ( 'NONE', #18552, .T. ) ;
#63338=AXIS2_PLACEMENT_3D ( 'NONE', #78402, #28300, #61175 ) ;
#63497=CARTESIAN_POINT ( 'NONE',  ( 0.000000000000000000, 0.000000000000000000, 0.000000000000000000 ) ) ;
#63758=PLANE ( 'NONE',  #49485 ) ;
#64275=UNCERTAINTY_MEASURE_WITH_UNIT (LENGTH_MEASURE( 1.000000000000000082E-05 ), #17440, 'distance_accuracy_value', 'NONE');
#64348=ORIENTED_EDGE ( 'NONE', *, *, #75385, .T. ) ;
#64397=ADVANCED_FACE ( 'NONE', ( #14338 ), #88784, .T. ) ;
#64785=LINE ( 'NONE', #47528, #36926 ) ;
#64803=DIRECTION ( 'NONE',  ( 0.000000000000000000, 0.000000000000000000, -1.000000000000000000 ) ) ;
#64932=ORIENTED_EDGE ( 'NONE', *, *, #50449, .F. ) ;
#64997=DIRECTION ( 'NONE',  ( 0.000000000000000000, 0.000000000000000000, -1.000000000000000000 ) ) ;
#65048=EDGE_CURVE ( 'NONE', #24916, #26344, #73243, .T. ) ;
#65183=ORIENTED_EDGE ( 'NONE', *, *, #71450, .F. ) ;
#65560=( NAMED_UNIT ( * ) PLANE_ANGLE_UNIT ( ) SI_UNIT ( $, .RADIAN. ) );
#66229=DIRECTION ( 'NONE',  ( 0.000000000000000000, 0.000000000000000000, -1.000000000000000000 ) ) ;
#66714=ADVANCED_FACE ( 'NONE', ( #38501, #30410 ), #41137, .T. ) ;
#67170=CIRCLE ( 'NONE', #36177, 4.000000000000000000 ) ;
#67258=ADVANCED_FACE ( 'NONE', ( #34943 ), #59200, .T. ) ;
#67835=CIRCLE ( 'NONE', #55718, 3.500000000000000000 ) ;
#68375=CARTESIAN_POINT ( 'NONE',  ( 0.000000000000000000, 4.000000000000000000, -2.000000000000000888 ) ) ;
#68576=UNCERTAINTY_MEASURE_WITH_UNIT (LENGTH_MEASURE( 1.000000000000000082E-05 ), #97149, 'distance_accuracy_value', 'NONE');
#69044=SURFACE_STYLE_FILL_AREA ( #58415 ) ;
#69077=CIRCLE ( 'NONE', #43192, 0.5000000000000000000 ) ;
#69361=ORIENTED_EDGE ( 'NONE', *, *, #49126, .T. ) ;
#69396=ORIENTED_EDGE ( 'NONE', *, *, #56417, .F. ) ;
#69616=TOROIDAL_SURFACE ( 'NONE', #35216, 3.500000000000000000, 0.5000000000000000000 ) ;
#70311=VERTEX_POINT ( 'NONE', #22914 ) ;
#70351=VERTEX_POINT ( 'NONE', #23987 ) ;
#70552=ADVANCED_FACE ( 'NONE', ( #7475 ), #38309, .T. ) ;
#71450=EDGE_CURVE ( 'NONE', #26344, #80736, #25812, .T. ) ;
#71584=AXIS2_PLACEMENT_3D ( 'NONE', #6294, #38701, #7360 ) ;
#72033=LINE ( 'NONE', #96848, #58777 ) ;
#72346=DIRECTION ( 'NONE',  ( 0.000000000000000000, 0.000000000000000000, 1.000000000000000000 ) ) ;
#72443=DIRECTION ( 'NONE',  ( -0.000000000000000000, -1.000000000000000000, -0.000000000000000000 ) ) ;
#72647=PRODUCT_DEFINITION_CONTEXT ( 'detailed design', #25254, 'design' ) ;
#73243=CIRCLE ( 'NONE', #97364, 4.000000000000000000 ) ;
#73477=CARTESIAN_POINT ( 'NONE',  ( 2.000000000000000888, 4.000000000000000000, 0.000000000000000000 ) ) ;
#73631=AXIS2_PLACEMENT_3D ( 'NONE', #76957, #92074, #12216 ) ;
#73637=CARTESIAN_POINT ( 'NONE',  ( 0.000000000000000000, 12.00000000000000000, 0.000000000000000000 ) ) ;
#74453=( NAMED_UNIT ( * ) PLANE_ANGLE_UNIT ( ) SI_UNIT ( $, .RADIAN. ) );
#74658=FACE_OUTER_BOUND ( 'NONE', #44169, .T. ) ;
#74695=FILL_AREA_STYLE_COLOUR ( '', #55829 ) ;
#74722=FACE_OUTER_BOUND ( 'NONE', #79468, .T. ) ;
#74931=AXIS2_PLACEMENT_3D ( 'NONE', #87150, #79042, #37564 ) ;
#75096=ORIENTED_EDGE ( 'NONE', *, *, #101860, .T. ) ;
#75385=EDGE_CURVE ( 'NONE', #80736, #70311, #82327, .T. ) ;
#75875=ORIENTED_EDGE ( 'NONE', *, *, #55231, .T. ) ;
#76442=COLOUR_RGB ( '', 0.66274510, 0.83137255, 0.94901961) ;
#76455=ORIENTED_EDGE ( 'NONE', *, *, #55803, .T. ) ;
#76767=UNCERTAINTY_MEASURE_WITH_UNIT (LENGTH_MEASURE( 1.000000000000000082E-05 ), #12915, 'distance_accuracy_value', 'NONE');
#76957=CARTESIAN_POINT ( 'NONE',  ( 0.000000000000000000, 0.000000000000000000, 0.000000000000000000 ) ) ;
#76983=COLOUR_RGB ( '', 0.31764706, 0.68627451, 0.89019608) ;
#77342=CARTESIAN_POINT ( 'NONE',  ( 0.000000000000000000, 0.5000000000000000000, 0.000000000000000000 ) ) ;
#77403=PRODUCT_DEFINITION_SHAPE ( 'NONE', 'NONE',  #6702 ) ;
#78280=DIRECTION ( 'NONE',  ( -0.000000000000000000, -1.000000000000000000, -0.000000000000000000 ) ) ;
#78402=CARTESIAN_POINT ( 'NONE',  ( 4.286263797015736595E-16, 0.5000000000000000000, 3.500000000000000000 ) ) ;
#78784=CARTESIAN_POINT ( 'NONE',  ( 0.000000000000000000, 0.5000000000000000000, -4.000000000000000000 ) ) ;
#78988=DIRECTION ( 'NONE',  ( 0.000000000000000000, 0.000000000000000000, -1.000000000000000000 ) ) ;
#79042=DIRECTION ( 'NONE',  ( -0.000000000000000000, -1.000000000000000000, -0.000000000000000000 ) ) ;
#79254=FILL_AREA_STYLE_COLOUR ( '', #4386 ) ;
#79372=FACE_OUTER_BOUND ( 'NONE', #41350, .T. ) ;
#79385=AXIS2_PLACEMENT_3D ( 'NONE', #51192, #17797, #106778 ) ;
#79468=EDGE_LOOP ( 'NONE', ( #104864, #105019, #76455, #34895 ) ) ;
#80610=EDGE_LOOP ( 'NONE', ( #6882, #69361 ) ) ;
#80688=EDGE_LOOP ( 'NONE', ( #10370, #57475, #29777, #101635 ) ) ;
#80736=VERTEX_POINT ( 'NONE', #95256 ) ;
#80954=SURFACE_STYLE_USAGE ( .BOTH. , #7587 ) ;
#81699=EDGE_CURVE ( 'NONE', #26344, #24916, #7082, .T. ) ;
#82029=ADVANCED_BREP_SHAPE_REPRESENTATION ( '', ( #87940, #10728 ), #26637 ) ;
#82132=CARTESIAN_POINT ( 'NONE',  ( 2.449293598294707400E-16, 4.000000000000000000, 2.000000000000000888 ) ) ;
#82327=CIRCLE ( 'NONE', #35884, 3.500000000000000000 ) ;
#82406=EDGE_CURVE ( 'NONE', #58206, #91320, #96801, .T. ) ;
#82560=PRESENTATION_STYLE_ASSIGNMENT (( #80954 ) ) ;
#82768=SURFACE_STYLE_USAGE ( .BOTH. , #101618 ) ;
#83222=( GEOMETRIC_REPRESENTATION_CONTEXT ( 3 ) GLOBAL_UNCERTAINTY_ASSIGNED_CONTEXT ( ( #64275 ) ) GLOBAL_UNIT_ASSIGNED_CONTEXT ( ( #17440, #50308, #62024 ) ) REPRESENTATION_CONTEXT ( 'NONE', 'WORKASPACE' ) );
#83357=SURFACE_STYLE_FILL_AREA ( #42369 ) ;
#83427=EDGE_CURVE ( 'NONE', #24916, #94714, #7969, .T. ) ;
#83727=DIRECTION ( 'NONE',  ( -0.000000000000000000, -1.000000000000000000, -0.000000000000000000 ) ) ;
#83778=CYLINDRICAL_SURFACE ( 'NONE', #71584, 2.000000000000000444 ) ;
#83909=AXIS2_PLACEMENT_3D ( 'NONE', #31765, #24217, #66229 ) ;
#83970=DIRECTION ( 'NONE',  ( -0.000000000000000000, -1.000000000000000000, -0.000000000000000000 ) ) ;
#84472=UNCERTAINTY_MEASURE_WITH_UNIT (LENGTH_MEASURE( 1.000000000000000082E-05 ), #56380, 'distance_accuracy_value', 'NONE');
#84976=EDGE_CURVE ( 'NONE', #10091, #35053, #67835, .T. ) ;
#85226=CIRCLE ( 'NONE', #19842, 0.5000000000000000000 ) ;
#85627=TOROIDAL_SURFACE ( 'NONE', #97599, 3.500000000000000000, 0.5000000000000000000 ) ;
#85765=DIRECTION ( 'NONE',  ( 0.000000000000000000, 0.000000000000000000, 1.000000000000000000 ) ) ;
#85773=CIRCLE ( 'NONE', #30730, 3.500000000000000000 ) ;
#86035=CARTESIAN_POINT ( 'NONE',  ( 0.000000000000000000, 4.000000000000000000, 0.000000000000000000 ) ) ;
#86861=ADVANCED_FACE ( 'NONE', ( #98546 ), #1437, .T. ) ;
#87150=CARTESIAN_POINT ( 'NONE',  ( 0.000000000000000000, 4.000000000000000000, 0.000000000000000000 ) ) ;
#87235=DIRECTION ( 'NONE',  ( -0.000000000000000000, -1.000000000000000000, -0.000000000000000000 ) ) ;
#87379=DIRECTION ( 'NONE',  ( 0.000000000000000000, 0.000000000000000000, 1.000000000000000000 ) ) ;
#87940=MANIFOLD_SOLID_BREP ( 'Fillet1', #103219 ) ;
#88204=DIRECTION ( 'NONE',  ( 1.000000000000000000, -0.000000000000000000, 1.224646799147353207E-16 ) ) ;
#88539=DIRECTION ( 'NONE',  ( -0.000000000000000000, -1.000000000000000000, -0.000000000000000000 ) ) ;
#88556=CARTESIAN_POINT ( 'NONE',  ( 4.000000000000000888, 2.111459998529851557E-18, 0.000000000000000000 ) ) ;
#88784=PLANE ( 'NONE',  #102772 ) ;
#88968=EDGE_CURVE ( 'NONE', #96436, #70351, #26979, .T. ) ;
#89489=DIRECTION ( 'NONE',  ( -0.000000000000000000, -1.000000000000000000, -0.000000000000000000 ) ) ;
#90213=DIRECTION ( 'NONE',  ( 0.000000000000000000, 1.000000000000000000, 0.000000000000000000 ) ) ;
#90237=STYLED_ITEM ( 'NONE', ( #82560 ), #55172 ) ;
#91320=VERTEX_POINT ( 'NONE', #82132 ) ;
#91918=ORIENTED_EDGE ( 'NONE', *, *, #12154, .T. ) ;
#92074=DIRECTION ( 'NONE',  ( -0.000000000000000000, -1.000000000000000000, -0.000000000000000000 ) ) ;
#92208=( GEOMETRIC_REPRESENTATION_CONTEXT ( 3 ) GLOBAL_UNCERTAINTY_ASSIGNED_CONTEXT ( ( #76767 ) ) GLOBAL_UNIT_ASSIGNED_CONTEXT ( ( #12915, #53401, #37780 ) ) REPRESENTATION_CONTEXT ( 'NONE', 'WORKASPACE' ) );
#92454=( GEOMETRIC_REPRESENTATION_CONTEXT ( 3 ) GLOBAL_UNCERTAINTY_ASSIGNED_CONTEXT ( ( #3018 ) ) GLOBAL_UNIT_ASSIGNED_CONTEXT ( ( #42303, #54622, #21788 ) ) REPRESENTATION_CONTEXT ( 'NONE', 'WORKASPACE' ) );
#92515=ORIENTED_EDGE ( 'NONE', *, *, #39415, .T. ) ;
#93761=DIRECTION ( 'NONE',  ( 0.000000000000000000, 1.000000000000000000, 0.000000000000000000 ) ) ;
#94490=CARTESIAN_POINT ( 'NONE',  ( 4.898587196589412829E-16, 0.000000000000000000, 4.000000000000000000 ) ) ;
#94714=VERTEX_POINT ( 'NONE', #78784 ) ;
#94842=EDGE_LOOP ( 'NONE', ( #103248, #92515, #99831, #104388 ) ) ;
#94937=SURFACE_SIDE_STYLE ('',( #22109 ) ) ;
#95189=ORIENTED_EDGE ( 'NONE', *, *, #50449, .T. ) ;
#95256=CARTESIAN_POINT ( 'NONE',  ( 0.000000000000000000, 4.000000000000000000, 3.500000000000000000 ) ) ;
#95271=VECTOR ( 'NONE', #33346, 1000.000000000000000 ) ;
#95993=DIRECTION ( 'NONE',  ( 0.000000000000000000, 0.000000000000000000, -1.000000000000000000 ) ) ;
#96137=ORIENTED_EDGE ( 'NONE', *, *, #65048, .F. ) ;
#96436=VERTEX_POINT ( 'NONE', #47639 ) ;
#96801=CIRCLE ( 'NONE', #5480, 2.000000000000000888 ) ;
#96848=CARTESIAN_POINT ( 'NONE',  ( 2.449293598294706907E-16, 0.000000000000000000, 2.000000000000000444 ) ) ;
#96894=ORIENTED_EDGE ( 'NONE', *, *, #55803, .F. ) ;
#97142=DIRECTION ( 'NONE',  ( 0.000000000000000000, 1.000000000000000000, 0.000000000000000000 ) ) ;
#97149=( LENGTH_UNIT ( ) NAMED_UNIT ( * ) SI_UNIT ( .MILLI., .METRE. ) );
#97364=AXIS2_PLACEMENT_3D ( 'NONE', #50821, #83727, #98333 ) ;
#97549=CIRCLE ( 'NONE', #54516, 4.000000000000000000 ) ;
#97599=AXIS2_PLACEMENT_3D ( 'NONE', #77342, #13648, #5565 ) ;
#98333=DIRECTION ( 'NONE',  ( 0.000000000000000000, 0.000000000000000000, 1.000000000000000000 ) ) ;
#98449=SHAPE_REPRESENTATION_RELATIONSHIP ( 'NONE' , 'NONE' ,  #22031, #82029 ) ;
#98546=FACE_OUTER_BOUND ( 'NONE', #100586, .T. ) ;
#98965=FILL_AREA_STYLE ('',( #74695 ) ) ;
#99289=( GEOMETRIC_REPRESENTATION_CONTEXT ( 3 ) GLOBAL_UNCERTAINTY_ASSIGNED_CONTEXT ( ( #68576 ) ) GLOBAL_UNIT_ASSIGNED_CONTEXT ( ( #97149, #37516, #46105 ) ) REPRESENTATION_CONTEXT ( 'NONE', 'WORKASPACE' ) );
#99831=ORIENTED_EDGE ( 'NONE', *, *, #100801, .T. ) ;
#99881=ORIENTED_EDGE ( 'NONE', *, *, #49126, .F. ) ;
#99906=ORIENTED_EDGE ( 'NONE', *, *, #75385, .F. ) ;
#100586=EDGE_LOOP ( 'NONE', ( #64932, #22099, #75875, #99881 ) ) ;
#100801=EDGE_CURVE ( 'NONE', #49975, #94714, #97549, .T. ) ;
#101618=SURFACE_SIDE_STYLE ('',( #35858 ) ) ;
#101635=ORIENTED_EDGE ( 'NONE', *, *, #48711, .T. ) ;
#101860=EDGE_CURVE ( 'NONE', #49975, #10091, #34096, .T. ) ;
#102408=APPLICATION_CONTEXT ( 'automotive_design' ) ;
#102459=FILL_AREA_STYLE_COLOUR ( '', #59149 ) ;
#102772=AXIS2_PLACEMENT_3D ( 'NONE', #73637, #24600, #38656 ) ;
#102791=STYLED_ITEM ( 'NONE', ( #19743 ), #3575 ) ;
#102810=CARTESIAN_POINT ( 'NONE',  ( 4.592425496802573972E-16, 0.000000000000000000, 3.500000000000000000 ) ) ;
#103219=CLOSED_SHELL ( 'NONE', ( #55172, #23880, #67258, #56944, #60242, #64397, #86861, #66714, #70552, #3575, #54542 ) ) ;
#103248=ORIENTED_EDGE ( 'NONE', *, *, #65048, .T. ) ;
#103443=ORIENTED_EDGE ( 'NONE', *, *, #82406, .F. ) ;
#104232=STYLED_ITEM ( 'NONE', ( #61507 ), #87940 ) ;
#104388=ORIENTED_EDGE ( 'NONE', *, *, #83427, .F. ) ;
#104621=DIRECTION ( 'NONE',  ( 0.000000000000000000, 0.000000000000000000, -1.000000000000000000 ) ) ;
#104864=ORIENTED_EDGE ( 'NONE', *, *, #101860, .F. ) ;
#104940=DIRECTION ( 'NONE',  ( -0.000000000000000000, -1.000000000000000000, -0.000000000000000000 ) ) ;
#105019=ORIENTED_EDGE ( 'NONE', *, *, #48711, .F. ) ;
#105248=( NAMED_UNIT ( * ) SI_UNIT ( $, .STERADIAN. ) SOLID_ANGLE_UNIT ( ) );
#105776=CARTESIAN_POINT ( 'NONE',  ( 0.000000000000000000, 0.5000000000000000000, 0.000000000000000000 ) ) ;
#106538=( NAMED_UNIT ( * ) SI_UNIT ( $, .STERADIAN. ) SOLID_ANGLE_UNIT ( ) );
#106688=ORIENTED_EDGE ( 'NONE', *, *, #12154, .F. ) ;
#106778=DIRECTION ( 'NONE',  ( 0.000000000000000000, 0.000000000000000000, 1.000000000000000000 ) ) ;
ENDSEC;
END-ISO-10303-21;
